ISO-10303-21;
HEADER;
/* Generated by software containing ST-Developer
 * from STEP Tools, Inc. (www.steptools.com) 
 */

FILE_DESCRIPTION(
/* description */ ('Four-valve pipe header'),
/* implementation_level */ '2;1');

FILE_NAME(
/* name */ 'Cap Screw - M4x16.step',
/* time_stamp */ '2026-10-29T16:56:19-07:00',
/* author */ (''),
/* organization */ (''),
/* preprocessor_version */ 'ST-DEVELOPER v20.2',
/* originating_system */ 'Autodesk Translation Framework v15.17.0.0',
/* authorisation */ '');

FILE_SCHEMA (('AUTOMOTIVE_DESIGN { 1 0 10303 214 3 1 1 }'));
ENDSEC;

DATA;
#10=MECHANICAL_DESIGN_GEOMETRIC_PRESENTATION_REPRESENTATION('',(#351),#10119);
#236=ORIENTED_CLOSED_SHELL('',*,#5599,.F.);
#239=BREP_WITH_VOIDS('Body1',#5598,(#236));
#274=CONICAL_SURFACE('',#6381,0.325,0.785398163397448);
#275=CONICAL_SURFACE('',#6385,0.335,0.785398163397448);
#276=CONICAL_SURFACE('',#6389,0.21,0.463647609000806);
#277=CONICAL_SURFACE('',#6393,0.18,0.785398163397448);
#299=SHAPE_REPRESENTATION_RELATIONSHIP('SRR','None',#10261,#325);
#325=ADVANCED_BREP_SHAPE_REPRESENTATION('',(#239),#10110);
#351=STYLED_ITEM('',(#10477),#239);
#525=FACE_BOUND('',#1430,.T.);
#680=PLANE('',#6379);
#681=PLANE('',#6387);
#682=PLANE('',#6395);
#683=PLANE('',#6396);
#684=PLANE('',#6397);
#685=PLANE('',#6398);
#686=PLANE('',#6399);
#687=PLANE('',#6400);
#688=PLANE('',#6401);
#689=PLANE('',#6402);
#690=PLANE('',#6403);
#994=FACE_OUTER_BOUND('',#1425,.T.);
#995=FACE_OUTER_BOUND('',#1426,.T.);
#996=FACE_OUTER_BOUND('',#1427,.T.);
#997=FACE_OUTER_BOUND('',#1428,.T.);
#998=FACE_OUTER_BOUND('',#1429,.T.);
#999=FACE_OUTER_BOUND('',#1431,.T.);
#1000=FACE_OUTER_BOUND('',#1432,.T.);
#1001=FACE_OUTER_BOUND('',#1433,.T.);
#1002=FACE_OUTER_BOUND('',#1434,.T.);
#1003=FACE_OUTER_BOUND('',#1435,.T.);
#1004=FACE_OUTER_BOUND('',#1436,.T.);
#1005=FACE_OUTER_BOUND('',#1437,.T.);
#1006=FACE_OUTER_BOUND('',#1438,.T.);
#1007=FACE_OUTER_BOUND('',#1439,.T.);
#1008=FACE_OUTER_BOUND('',#1440,.T.);
#1009=FACE_OUTER_BOUND('',#1441,.T.);
#1010=FACE_OUTER_BOUND('',#1442,.T.);
#1425=EDGE_LOOP('',(#4809));
#1426=EDGE_LOOP('',(#4810,#4811,#4812,#4813));
#1427=EDGE_LOOP('',(#4814,#4815,#4816,#4817));
#1428=EDGE_LOOP('',(#4818,#4819,#4820,#4821));
#1429=EDGE_LOOP('',(#4822));
#1430=EDGE_LOOP('',(#4823));
#1431=EDGE_LOOP('',(#4824,#4825,#4826,#4827));
#1432=EDGE_LOOP('',(#4828,#4829,#4830,#4831));
#1433=EDGE_LOOP('',(#4832,#4833,#4834,#4835));
#1434=EDGE_LOOP('',(#4836));
#1435=EDGE_LOOP('',(#4837,#4838,#4839,#4840));
#1436=EDGE_LOOP('',(#4841,#4842,#4843,#4844));
#1437=EDGE_LOOP('',(#4845,#4846,#4847,#4848));
#1438=EDGE_LOOP('',(#4849,#4850,#4851,#4852));
#1439=EDGE_LOOP('',(#4853,#4854,#4855,#4856));
#1440=EDGE_LOOP('',(#4857,#4858,#4859,#4860));
#1441=EDGE_LOOP('',(#4861,#4862,#4863,#4864,#4865,#4866));
#1442=EDGE_LOOP('',(#4867,#4868,#4869,#4870,#4871,#4872));
#1809=LINE('',#9636,#2227);
#1810=LINE('',#9640,#2228);
#1811=LINE('',#9644,#2229);
#1812=LINE('',#9651,#2230);
#1813=LINE('',#9655,#2231);
#1814=LINE('',#9659,#2232);
#1815=LINE('',#9664,#2233);
#1816=LINE('',#9666,#2234);
#1817=LINE('',#9668,#2235);
#1818=LINE('',#9669,#2236);
#1819=LINE('',#9672,#2237);
#1820=LINE('',#9674,#2238);
#1821=LINE('',#9675,#2239);
#1822=LINE('',#9678,#2240);
#1823=LINE('',#9680,#2241);
#1824=LINE('',#9681,#2242);
#1825=LINE('',#9684,#2243);
#1826=LINE('',#9686,#2244);
#1827=LINE('',#9687,#2245);
#1828=LINE('',#9690,#2246);
#1829=LINE('',#9692,#2247);
#1830=LINE('',#9693,#2248);
#1831=LINE('',#9695,#2249);
#1832=LINE('',#9696,#2250);
#2227=VECTOR('',#7834,0.325);
#2228=VECTOR('',#7839,0.35);
#2229=VECTOR('',#7844,0.335);
#2230=VECTOR('',#7853,0.21);
#2231=VECTOR('',#7858,0.2);
#2232=VECTOR('',#7863,0.18);
#2233=VECTOR('',#7868,1.);
#2234=VECTOR('',#7869,1.);
#2235=VECTOR('',#7870,1.);
#2236=VECTOR('',#7871,1.);
#2237=VECTOR('',#7874,1.);
#2238=VECTOR('',#7875,1.);
#2239=VECTOR('',#7876,1.);
#2240=VECTOR('',#7879,1.);
#2241=VECTOR('',#7880,1.);
#2242=VECTOR('',#7881,1.);
#2243=VECTOR('',#7884,1.);
#2244=VECTOR('',#7885,1.);
#2245=VECTOR('',#7886,1.);
#2246=VECTOR('',#7889,1.);
#2247=VECTOR('',#7890,1.);
#2248=VECTOR('',#7891,1.);
#2249=VECTOR('',#7894,1.);
#2250=VECTOR('',#7895,1.);
#2539=CIRCLE('',#6380,0.3);
#2540=CIRCLE('',#6382,0.35);
#2541=CIRCLE('',#6384,0.35);
#2542=CIRCLE('',#6386,0.32);
#2543=CIRCLE('',#6388,0.22);
#2544=CIRCLE('',#6390,0.1954);
#2545=CIRCLE('',#6392,0.1954);
#2546=CIRCLE('',#6394,0.16);
#2928=VERTEX_POINT('',#9631);
#2929=VERTEX_POINT('',#9634);
#2930=VERTEX_POINT('',#9638);
#2931=VERTEX_POINT('',#9642);
#2932=VERTEX_POINT('',#9646);
#2933=VERTEX_POINT('',#9649);
#2934=VERTEX_POINT('',#9653);
#2935=VERTEX_POINT('',#9657);
#2936=VERTEX_POINT('',#9662);
#2937=VERTEX_POINT('',#9663);
#2938=VERTEX_POINT('',#9665);
#2939=VERTEX_POINT('',#9667);
#2940=VERTEX_POINT('',#9671);
#2941=VERTEX_POINT('',#9673);
#2942=VERTEX_POINT('',#9677);
#2943=VERTEX_POINT('',#9679);
#2944=VERTEX_POINT('',#9683);
#2945=VERTEX_POINT('',#9685);
#2946=VERTEX_POINT('',#9689);
#2947=VERTEX_POINT('',#9691);
#3571=EDGE_CURVE('',#2928,#2928,#2539,.T.);
#3572=EDGE_CURVE('',#2929,#2929,#2540,.T.);
#3573=EDGE_CURVE('',#2929,#2928,#1809,.T.);
#3574=EDGE_CURVE('',#2930,#2930,#2541,.T.);
#3575=EDGE_CURVE('',#2930,#2929,#1810,.T.);
#3576=EDGE_CURVE('',#2931,#2931,#2542,.T.);
#3577=EDGE_CURVE('',#2931,#2930,#1811,.T.);
#3578=EDGE_CURVE('',#2932,#2932,#2543,.T.);
#3579=EDGE_CURVE('',#2933,#2933,#2544,.F.);
#3580=EDGE_CURVE('',#2933,#2932,#1812,.T.);
#3581=EDGE_CURVE('',#2934,#2934,#2545,.F.);
#3582=EDGE_CURVE('',#2934,#2933,#1813,.T.);
#3583=EDGE_CURVE('',#2935,#2935,#2546,.T.);
#3584=EDGE_CURVE('',#2935,#2934,#1814,.T.);
#3585=EDGE_CURVE('',#2936,#2937,#1815,.T.);
#3586=EDGE_CURVE('',#2937,#2938,#1816,.T.);
#3587=EDGE_CURVE('',#2938,#2939,#1817,.T.);
#3588=EDGE_CURVE('',#2936,#2939,#1818,.T.);
#3589=EDGE_CURVE('',#2937,#2940,#1819,.T.);
#3590=EDGE_CURVE('',#2940,#2941,#1820,.T.);
#3591=EDGE_CURVE('',#2941,#2938,#1821,.T.);
#3592=EDGE_CURVE('',#2940,#2942,#1822,.T.);
#3593=EDGE_CURVE('',#2942,#2943,#1823,.T.);
#3594=EDGE_CURVE('',#2943,#2941,#1824,.T.);
#3595=EDGE_CURVE('',#2942,#2944,#1825,.T.);
#3596=EDGE_CURVE('',#2944,#2945,#1826,.T.);
#3597=EDGE_CURVE('',#2945,#2943,#1827,.T.);
#3598=EDGE_CURVE('',#2944,#2946,#1828,.T.);
#3599=EDGE_CURVE('',#2946,#2947,#1829,.T.);
#3600=EDGE_CURVE('',#2947,#2945,#1830,.T.);
#3601=EDGE_CURVE('',#2946,#2936,#1831,.T.);
#3602=EDGE_CURVE('',#2939,#2947,#1832,.T.);
#4809=ORIENTED_EDGE('',*,*,#3571,.F.);
#4810=ORIENTED_EDGE('',*,*,#3572,.F.);
#4811=ORIENTED_EDGE('',*,*,#3573,.T.);
#4812=ORIENTED_EDGE('',*,*,#3571,.T.);
#4813=ORIENTED_EDGE('',*,*,#3573,.F.);
#4814=ORIENTED_EDGE('',*,*,#3574,.F.);
#4815=ORIENTED_EDGE('',*,*,#3575,.T.);
#4816=ORIENTED_EDGE('',*,*,#3572,.T.);
#4817=ORIENTED_EDGE('',*,*,#3575,.F.);
#4818=ORIENTED_EDGE('',*,*,#3576,.F.);
#4819=ORIENTED_EDGE('',*,*,#3577,.T.);
#4820=ORIENTED_EDGE('',*,*,#3574,.T.);
#4821=ORIENTED_EDGE('',*,*,#3577,.F.);
#4822=ORIENTED_EDGE('',*,*,#3576,.T.);
#4823=ORIENTED_EDGE('',*,*,#3578,.F.);
#4824=ORIENTED_EDGE('',*,*,#3579,.F.);
#4825=ORIENTED_EDGE('',*,*,#3580,.T.);
#4826=ORIENTED_EDGE('',*,*,#3578,.T.);
#4827=ORIENTED_EDGE('',*,*,#3580,.F.);
#4828=ORIENTED_EDGE('',*,*,#3581,.F.);
#4829=ORIENTED_EDGE('',*,*,#3582,.T.);
#4830=ORIENTED_EDGE('',*,*,#3579,.T.);
#4831=ORIENTED_EDGE('',*,*,#3582,.F.);
#4832=ORIENTED_EDGE('',*,*,#3583,.F.);
#4833=ORIENTED_EDGE('',*,*,#3584,.T.);
#4834=ORIENTED_EDGE('',*,*,#3581,.T.);
#4835=ORIENTED_EDGE('',*,*,#3584,.F.);
#4836=ORIENTED_EDGE('',*,*,#3583,.T.);
#4837=ORIENTED_EDGE('',*,*,#3585,.T.);
#4838=ORIENTED_EDGE('',*,*,#3586,.T.);
#4839=ORIENTED_EDGE('',*,*,#3587,.T.);
#4840=ORIENTED_EDGE('',*,*,#3588,.F.);
#4841=ORIENTED_EDGE('',*,*,#3589,.T.);
#4842=ORIENTED_EDGE('',*,*,#3590,.T.);
#4843=ORIENTED_EDGE('',*,*,#3591,.T.);
#4844=ORIENTED_EDGE('',*,*,#3586,.F.);
#4845=ORIENTED_EDGE('',*,*,#3592,.T.);
#4846=ORIENTED_EDGE('',*,*,#3593,.T.);
#4847=ORIENTED_EDGE('',*,*,#3594,.T.);
#4848=ORIENTED_EDGE('',*,*,#3590,.F.);
#4849=ORIENTED_EDGE('',*,*,#3595,.T.);
#4850=ORIENTED_EDGE('',*,*,#3596,.T.);
#4851=ORIENTED_EDGE('',*,*,#3597,.T.);
#4852=ORIENTED_EDGE('',*,*,#3593,.F.);
#4853=ORIENTED_EDGE('',*,*,#3598,.T.);
#4854=ORIENTED_EDGE('',*,*,#3599,.T.);
#4855=ORIENTED_EDGE('',*,*,#3600,.T.);
#4856=ORIENTED_EDGE('',*,*,#3596,.F.);
#4857=ORIENTED_EDGE('',*,*,#3601,.T.);
#4858=ORIENTED_EDGE('',*,*,#3588,.T.);
#4859=ORIENTED_EDGE('',*,*,#3602,.T.);
#4860=ORIENTED_EDGE('',*,*,#3599,.F.);
#4861=ORIENTED_EDGE('',*,*,#3601,.F.);
#4862=ORIENTED_EDGE('',*,*,#3598,.F.);
#4863=ORIENTED_EDGE('',*,*,#3595,.F.);
#4864=ORIENTED_EDGE('',*,*,#3592,.F.);
#4865=ORIENTED_EDGE('',*,*,#3589,.F.);
#4866=ORIENTED_EDGE('',*,*,#3585,.F.);
#4867=ORIENTED_EDGE('',*,*,#3602,.F.);
#4868=ORIENTED_EDGE('',*,*,#3587,.F.);
#4869=ORIENTED_EDGE('',*,*,#3591,.F.);
#4870=ORIENTED_EDGE('',*,*,#3594,.F.);
#4871=ORIENTED_EDGE('',*,*,#3597,.F.);
#4872=ORIENTED_EDGE('',*,*,#3600,.F.);
#5237=CYLINDRICAL_SURFACE('',#6383,0.35);
#5238=CYLINDRICAL_SURFACE('',#6391,0.1954);
#5494=ADVANCED_FACE('',(#994),#680,.T.);
#5495=ADVANCED_FACE('',(#995),#274,.T.);
#5496=ADVANCED_FACE('',(#996),#5237,.T.);
#5497=ADVANCED_FACE('',(#997),#275,.T.);
#5498=ADVANCED_FACE('',(#998,#525),#681,.T.);
#5499=ADVANCED_FACE('',(#999),#276,.T.);
#5500=ADVANCED_FACE('',(#1000),#5238,.T.);
#5501=ADVANCED_FACE('',(#1001),#277,.T.);
#5502=ADVANCED_FACE('',(#1002),#682,.T.);
#5503=ADVANCED_FACE('',(#1003),#683,.F.);
#5504=ADVANCED_FACE('',(#1004),#684,.F.);
#5505=ADVANCED_FACE('',(#1005),#685,.F.);
#5506=ADVANCED_FACE('',(#1006),#686,.F.);
#5507=ADVANCED_FACE('',(#1007),#687,.F.);
#5508=ADVANCED_FACE('',(#1008),#688,.F.);
#5509=ADVANCED_FACE('',(#1009),#689,.F.);
#5510=ADVANCED_FACE('',(#1010),#690,.F.);
#5598=CLOSED_SHELL('',(#5494,#5495,#5496,#5497,#5498,#5499,#5500,#5501,
#5502));
#5599=CLOSED_SHELL('',(#5503,#5504,#5505,#5506,#5507,#5508,#5509,#5510));
#6378=AXIS2_PLACEMENT_3D('',#9629,#7824,#7825);
#6379=AXIS2_PLACEMENT_3D('',#9630,#7826,#7827);
#6380=AXIS2_PLACEMENT_3D('',#9632,#7828,#7829);
#6381=AXIS2_PLACEMENT_3D('',#9633,#7830,#7831);
#6382=AXIS2_PLACEMENT_3D('',#9635,#7832,#7833);
#6383=AXIS2_PLACEMENT_3D('',#9637,#7835,#7836);
#6384=AXIS2_PLACEMENT_3D('',#9639,#7837,#7838);
#6385=AXIS2_PLACEMENT_3D('',#9641,#7840,#7841);
#6386=AXIS2_PLACEMENT_3D('',#9643,#7842,#7843);
#6387=AXIS2_PLACEMENT_3D('',#9645,#7845,#7846);
#6388=AXIS2_PLACEMENT_3D('',#9647,#7847,#7848);
#6389=AXIS2_PLACEMENT_3D('',#9648,#7849,#7850);
#6390=AXIS2_PLACEMENT_3D('',#9650,#7851,#7852);
#6391=AXIS2_PLACEMENT_3D('',#9652,#7854,#7855);
#6392=AXIS2_PLACEMENT_3D('',#9654,#7856,#7857);
#6393=AXIS2_PLACEMENT_3D('',#9656,#7859,#7860);
#6394=AXIS2_PLACEMENT_3D('',#9658,#7861,#7862);
#6395=AXIS2_PLACEMENT_3D('',#9660,#7864,#7865);
#6396=AXIS2_PLACEMENT_3D('',#9661,#7866,#7867);
#6397=AXIS2_PLACEMENT_3D('',#9670,#7872,#7873);
#6398=AXIS2_PLACEMENT_3D('',#9676,#7877,#7878);
#6399=AXIS2_PLACEMENT_3D('',#9682,#7882,#7883);
#6400=AXIS2_PLACEMENT_3D('',#9688,#7887,#7888);
#6401=AXIS2_PLACEMENT_3D('',#9694,#7892,#7893);
#6402=AXIS2_PLACEMENT_3D('',#9697,#7896,#7897);
#6403=AXIS2_PLACEMENT_3D('',#9698,#7898,#7899);
#7824=DIRECTION('axis',(0.,0.,1.));
#7825=DIRECTION('refdir',(1.,0.,0.));
#7826=DIRECTION('center_axis',(0.,1.,0.));
#7827=DIRECTION('ref_axis',(0.,0.,1.));
#7828=DIRECTION('center_axis',(0.,-1.,0.));
#7829=DIRECTION('ref_axis',(1.,0.,0.));
#7830=DIRECTION('center_axis',(0.,-1.,0.));
#7831=DIRECTION('ref_axis',(1.,0.,0.));
#7832=DIRECTION('center_axis',(0.,-1.,0.));
#7833=DIRECTION('ref_axis',(1.,0.,0.));
#7834=DIRECTION('',(0.707106781186547,0.707106781186548,8.65956056235493E-17));
#7835=DIRECTION('center_axis',(0.,-1.,0.));
#7836=DIRECTION('ref_axis',(1.,0.,0.));
#7837=DIRECTION('center_axis',(0.,-1.,0.));
#7838=DIRECTION('ref_axis',(1.,0.,0.));
#7839=DIRECTION('',(0.,1.,0.));
#7840=DIRECTION('center_axis',(0.,1.,0.));
#7841=DIRECTION('ref_axis',(1.,0.,0.));
#7842=DIRECTION('center_axis',(0.,-1.,0.));
#7843=DIRECTION('ref_axis',(1.,0.,0.));
#7844=DIRECTION('',(-0.707106781186547,0.707106781186548,-8.65956056235493E-17));
#7845=DIRECTION('center_axis',(0.,-1.,0.));
#7846=DIRECTION('ref_axis',(0.,0.,-1.));
#7847=DIRECTION('center_axis',(0.,-1.,0.));
#7848=DIRECTION('ref_axis',(1.,0.,0.));
#7849=DIRECTION('center_axis',(0.,1.,0.));
#7850=DIRECTION('ref_axis',(1.,0.,0.));
#7851=DIRECTION('center_axis',(0.,1.,0.));
#7852=DIRECTION('ref_axis',(1.,0.,0.));
#7853=DIRECTION('',(-0.447213595499958,0.894427190999916,-5.47678698264203E-17));
#7854=DIRECTION('center_axis',(0.,-1.,0.));
#7855=DIRECTION('ref_axis',(1.,0.,0.));
#7856=DIRECTION('center_axis',(0.,1.,0.));
#7857=DIRECTION('ref_axis',(1.,0.,0.));
#7858=DIRECTION('',(0.,1.,0.));
#7859=DIRECTION('center_axis',(0.,1.,0.));
#7860=DIRECTION('ref_axis',(1.,0.,0.));
#7861=DIRECTION('center_axis',(0.,-1.,0.));
#7862=DIRECTION('ref_axis',(1.,0.,0.));
#7863=DIRECTION('',(-0.707106781186547,0.707106781186548,-8.65956056235493E-17));
#7864=DIRECTION('center_axis',(0.,-1.,0.));
#7865=DIRECTION('ref_axis',(0.,0.,-1.));
#7866=DIRECTION('center_axis',(0.866025403784439,0.,-0.5));
#7867=DIRECTION('ref_axis',(0.5,0.,0.866025403784439));
#7868=DIRECTION('',(-0.5,0.,-0.866025403784439));
#7869=DIRECTION('',(0.,-1.,0.));
#7870=DIRECTION('',(0.5,0.,0.866025403784439));
#7871=DIRECTION('',(0.,-1.,0.));
#7872=DIRECTION('center_axis',(1.60246890531964E-16,0.,-1.));
#7873=DIRECTION('ref_axis',(1.,0.,1.60246890531964E-16));
#7874=DIRECTION('',(-1.,0.,-1.60246890531964E-16));
#7875=DIRECTION('',(0.,-1.,0.));
#7876=DIRECTION('',(1.,0.,1.60246890531964E-16));
#7877=DIRECTION('center_axis',(-0.866025403784439,0.,-0.5));
#7878=DIRECTION('ref_axis',(0.5,0.,-0.866025403784439));
#7879=DIRECTION('',(-0.5,0.,0.866025403784439));
#7880=DIRECTION('',(0.,-1.,0.));
#7881=DIRECTION('',(0.5,0.,-0.866025403784439));
#7882=DIRECTION('center_axis',(-0.866025403784439,0.,0.5));
#7883=DIRECTION('ref_axis',(-0.5,0.,-0.866025403784439));
#7884=DIRECTION('',(0.5,0.,0.866025403784439));
#7885=DIRECTION('',(0.,-1.,0.));
#7886=DIRECTION('',(-0.5,0.,-0.866025403784439));
#7887=DIRECTION('center_axis',(-1.60246890531964E-16,0.,1.));
#7888=DIRECTION('ref_axis',(-1.,0.,-1.60246890531964E-16));
#7889=DIRECTION('',(1.,0.,1.60246890531964E-16));
#7890=DIRECTION('',(0.,-1.,0.));
#7891=DIRECTION('',(-1.,0.,-1.60246890531964E-16));
#7892=DIRECTION('center_axis',(0.866025403784439,0.,0.5));
#7893=DIRECTION('ref_axis',(-0.5,0.,0.866025403784439));
#7894=DIRECTION('',(0.5,0.,-0.866025403784439));
#7895=DIRECTION('',(-0.5,0.,0.866025403784439));
#7896=DIRECTION('center_axis',(0.,1.,0.));
#7897=DIRECTION('ref_axis',(1.,0.,0.));
#7898=DIRECTION('center_axis',(0.,-1.,0.));
#7899=DIRECTION('ref_axis',(0.,0.,-1.));
#9629=CARTESIAN_POINT('',(0.,0.,0.));
#9630=CARTESIAN_POINT('Origin',(0.3,0.4,0.));
#9631=CARTESIAN_POINT('',(-0.3,0.4,-3.67394039744206E-17));
#9632=CARTESIAN_POINT('Origin',(0.,0.4,0.));
#9633=CARTESIAN_POINT('Origin',(0.,0.375,0.));
#9634=CARTESIAN_POINT('',(-0.35,0.35,-4.28626379701573E-17));
#9635=CARTESIAN_POINT('Origin',(0.,0.35,0.));
#9636=CARTESIAN_POINT('',(-0.325,0.375,-3.9801020972289E-17));
#9637=CARTESIAN_POINT('Origin',(0.,0.19,0.));
#9638=CARTESIAN_POINT('',(-0.35,0.03,-4.28626379701574E-17));
#9639=CARTESIAN_POINT('Origin',(0.,0.03,0.));
#9640=CARTESIAN_POINT('',(-0.35,0.19,-4.28626379701574E-17));
#9641=CARTESIAN_POINT('Origin',(0.,0.0149999999999999,0.));
#9642=CARTESIAN_POINT('',(-0.32,-3.29597460435593E-17,-3.91886975727153E-17));
#9643=CARTESIAN_POINT('Origin',(0.,0.,0.));
#9644=CARTESIAN_POINT('',(-0.335,0.0149999999999999,-4.10256677714363E-17));
#9645=CARTESIAN_POINT('Origin',(0.22,0.,0.));
#9646=CARTESIAN_POINT('',(-0.22,-6.93889390390723E-18,-2.69422295812418E-17));
#9647=CARTESIAN_POINT('Origin',(0.,0.,0.));
#9648=CARTESIAN_POINT('Origin',(0.,-0.02,0.));
#9649=CARTESIAN_POINT('',(-0.1954,-0.0492,2.39295984553393E-17));
#9650=CARTESIAN_POINT('Origin',(0.,-0.0492,0.));
#9651=CARTESIAN_POINT('',(-0.21,-0.02,-2.57175827820944E-17));
#9652=CARTESIAN_POINT('Origin',(0.,-0.8,0.));
#9653=CARTESIAN_POINT('',(-0.1954,-1.5646,2.39295984553393E-17));
#9654=CARTESIAN_POINT('Origin',(0.,-1.5646,0.));
#9655=CARTESIAN_POINT('',(-0.1954,-0.8,-2.39295984553393E-17));
#9656=CARTESIAN_POINT('Origin',(0.,-1.58,0.));
#9657=CARTESIAN_POINT('',(-0.16,-1.6,-1.95943487863577E-17));
#9658=CARTESIAN_POINT('Origin',(0.,-1.6,0.));
#9659=CARTESIAN_POINT('',(-0.18,-1.58,-2.20436423846524E-17));
#9660=CARTESIAN_POINT('Origin',(0.,-1.6,0.));
#9661=CARTESIAN_POINT('Origin',(0.0866025403784439,-0.4,-0.15));
#9662=CARTESIAN_POINT('',(0.173205080756888,-0.4,0.));
#9663=CARTESIAN_POINT('',(0.0866025403784439,-0.4,-0.15));
#9664=CARTESIAN_POINT('',(0.173205080756888,-0.4,0.));
#9665=CARTESIAN_POINT('',(0.0866025403784439,-0.64,-0.15));
#9666=CARTESIAN_POINT('',(0.0866025403784439,-0.4,-0.15));
#9667=CARTESIAN_POINT('',(0.173205080756888,-0.64,0.));
#9668=CARTESIAN_POINT('',(0.173205080756888,-0.64,0.));
#9669=CARTESIAN_POINT('',(0.173205080756888,-0.4,0.));
#9670=CARTESIAN_POINT('Origin',(-0.0866025403784438,-0.4,-0.15));
#9671=CARTESIAN_POINT('',(-0.0866025403784438,-0.4,-0.15));
#9672=CARTESIAN_POINT('',(0.0866025403784439,-0.4,-0.15));
#9673=CARTESIAN_POINT('',(-0.0866025403784438,-0.64,-0.15));
#9674=CARTESIAN_POINT('',(-0.0866025403784438,-0.4,-0.15));
#9675=CARTESIAN_POINT('',(0.0866025403784439,-0.64,-0.15));
#9676=CARTESIAN_POINT('Origin',(-0.173205080756888,-0.4,-2.77555756156289E-17));
#9677=CARTESIAN_POINT('',(-0.173205080756888,-0.4,-2.12115047744981E-17));
#9678=CARTESIAN_POINT('',(-0.0866025403784438,-0.4,-0.15));
#9679=CARTESIAN_POINT('',(-0.173205080756888,-0.64,-2.77555756156289E-17));
#9680=CARTESIAN_POINT('',(-0.173205080756888,-0.4,-2.12115047744981E-17));
#9681=CARTESIAN_POINT('',(-0.0866025403784438,-0.64,-0.15));
#9682=CARTESIAN_POINT('Origin',(-0.0866025403784439,-0.4,0.15));
#9683=CARTESIAN_POINT('',(-0.0866025403784439,-0.4,0.15));
#9684=CARTESIAN_POINT('',(-0.173205080756888,-0.4,-2.12115047744981E-17));
#9685=CARTESIAN_POINT('',(-0.0866025403784439,-0.64,0.15));
#9686=CARTESIAN_POINT('',(-0.0866025403784439,-0.4,0.15));
#9687=CARTESIAN_POINT('',(-0.173205080756888,-0.64,-2.12115047744981E-17));
#9688=CARTESIAN_POINT('Origin',(0.0866025403784439,-0.4,0.15));
#9689=CARTESIAN_POINT('',(0.0866025403784439,-0.4,0.15));
#9690=CARTESIAN_POINT('',(-0.0866025403784439,-0.4,0.15));
#9691=CARTESIAN_POINT('',(0.0866025403784439,-0.64,0.15));
#9692=CARTESIAN_POINT('',(0.0866025403784439,-0.4,0.15));
#9693=CARTESIAN_POINT('',(-0.0866025403784439,-0.64,0.15));
#9694=CARTESIAN_POINT('Origin',(0.173205080756888,-0.4,0.));
#9695=CARTESIAN_POINT('',(0.0866025403784439,-0.4,0.15));
#9696=CARTESIAN_POINT('',(0.0866025403784439,-0.64,0.15));
#9697=CARTESIAN_POINT('Origin',(0.,-0.4,-2.77555756156289E-17));
#9698=CARTESIAN_POINT('Origin',(0.,-0.64,-2.77555756156289E-17));
#10079=UNCERTAINTY_MEASURE_WITH_UNIT(LENGTH_MEASURE(0.001),#10120,
'DISTANCE_ACCURACY_VALUE',
'Maximum model space distance between geometric entities at asserted c
onnectivities');
#10088=UNCERTAINTY_MEASURE_WITH_UNIT(LENGTH_MEASURE(0.001),#10120,
'DISTANCE_ACCURACY_VALUE',
'Maximum model space distance between geometric entities at asserted c
onnectivities');
#10110=(
GEOMETRIC_REPRESENTATION_CONTEXT(3)
GLOBAL_UNCERTAINTY_ASSIGNED_CONTEXT((#10079))
GLOBAL_UNIT_ASSIGNED_CONTEXT((#10120,#10122,#10123))
REPRESENTATION_CONTEXT('','3D')
);
#10119=(
GEOMETRIC_REPRESENTATION_CONTEXT(3)
GLOBAL_UNCERTAINTY_ASSIGNED_CONTEXT((#10088))
GLOBAL_UNIT_ASSIGNED_CONTEXT((#10120,#10122,#10123))
REPRESENTATION_CONTEXT('','3D')
);
#10120=(
LENGTH_UNIT()
NAMED_UNIT(*)
SI_UNIT(.CENTI.,.METRE.)
);
#10122=(
NAMED_UNIT(*)
PLANE_ANGLE_UNIT()
SI_UNIT($,.RADIAN.)
);
#10123=(
NAMED_UNIT(*)
SI_UNIT($,.STERADIAN.)
SOLID_ANGLE_UNIT()
);
#10145=SHAPE_DEFINITION_REPRESENTATION(#10175,#10261);
#10175=PRODUCT_DEFINITION_SHAPE('',$,#10292);
#10261=SHAPE_REPRESENTATION('',(#6378),#10110);
#10270=PRODUCT_DEFINITION_CONTEXT('part definition',#10362,'design');
#10292=PRODUCT_DEFINITION('Cap Screw - M4x16','Cap Screw - M4x16',#10322,
#10270);
#10322=PRODUCT_DEFINITION_FORMATION('',$,#10385);
#10362=APPLICATION_CONTEXT(
'Core Data for Automotive Mechanical Design Process');
#10363=PRODUCT_CONTEXT('part definition',#10362,'mechanical');
#10385=PRODUCT('Cap Screw - M4x16','Cap Screw - M4x16',
'Cap Screw - M4x16',(#10363));
#10471=COLOUR_RGB('Black',0.12,0.14,0.17);
#10472=FILL_AREA_STYLE_COLOUR('',#10471);
#10473=FILL_AREA_STYLE('',(#10472));
#10474=SURFACE_STYLE_FILL_AREA(#10473);
#10475=SURFACE_SIDE_STYLE('',(#10474));
#10476=SURFACE_STYLE_USAGE(.BOTH.,#10475);
#10477=PRESENTATION_STYLE_ASSIGNMENT((#10476));
ENDSEC;
END-ISO-10303-21;
